ISO-10303-21;
HEADER;
/* Generated by software containing ST-Developer
 * from STEP Tools, Inc. (www.steptools.com) 
 */

FILE_DESCRIPTION(
/* description */ ('Manual piston pump'),
/* implementation_level */ '2;1');

FILE_NAME(
/* name */ 'Socket Set Screw - M4x6.step',
/* time_stamp */ '2026-11-02T16:54:23-08:00',
/* author */ (''),
/* organization */ (''),
/* preprocessor_version */ 'ST-DEVELOPER v20.2',
/* originating_system */ 'Autodesk Translation Framework v15.17.0.0',
/* authorisation */ '');

FILE_SCHEMA (('AUTOMOTIVE_DESIGN { 1 0 10303 214 3 1 1 }'));
ENDSEC;

DATA;
#10=MECHANICAL_DESIGN_GEOMETRIC_PRESENTATION_REPRESENTATION('',(#751),#19043);
#548=CONICAL_SURFACE('',#11347,0.185,0.785398163397449);
#549=CONICAL_SURFACE('',#11351,0.1625,0.785398163397449);
#617=SHAPE_REPRESENTATION_RELATIONSHIP('SRR','None',#19367,#680);
#680=ADVANCED_BREP_SHAPE_REPRESENTATION('',(#819),#19034);
#751=STYLED_ITEM('',(#19663),#819);
#819=MANIFOLD_SOLID_BREP('Body1',#9539);
#1032=FACE_BOUND('',#2584,.T.);
#1271=CYLINDRICAL_SURFACE('',#11349,0.1954);
#1796=FACE_OUTER_BOUND('',#2576,.T.);
#1797=FACE_OUTER_BOUND('',#2577,.T.);
#1798=FACE_OUTER_BOUND('',#2578,.T.);
#1799=FACE_OUTER_BOUND('',#2579,.T.);
#1800=FACE_OUTER_BOUND('',#2580,.T.);
#1801=FACE_OUTER_BOUND('',#2581,.T.);
#1802=FACE_OUTER_BOUND('',#2582,.T.);
#1803=FACE_OUTER_BOUND('',#2583,.T.);
#1804=FACE_OUTER_BOUND('',#2585,.T.);
#1805=FACE_OUTER_BOUND('',#2586,.T.);
#1806=FACE_OUTER_BOUND('',#2587,.T.);
#1807=FACE_OUTER_BOUND('',#2588,.T.);
#2576=EDGE_LOOP('',(#8301,#8302,#8303,#8304));
#2577=EDGE_LOOP('',(#8305,#8306,#8307,#8308));
#2578=EDGE_LOOP('',(#8309,#8310,#8311,#8312));
#2579=EDGE_LOOP('',(#8313,#8314,#8315,#8316));
#2580=EDGE_LOOP('',(#8317,#8318,#8319,#8320));
#2581=EDGE_LOOP('',(#8321,#8322,#8323,#8324));
#2582=EDGE_LOOP('',(#8325,#8326,#8327,#8328,#8329,#8330));
#2583=EDGE_LOOP('',(#8331));
#2584=EDGE_LOOP('',(#8332,#8333,#8334,#8335,#8336,#8337));
#2585=EDGE_LOOP('',(#8338,#8339,#8340,#8341));
#2586=EDGE_LOOP('',(#8342,#8343,#8344,#8345));
#2587=EDGE_LOOP('',(#8346,#8347,#8348,#8349));
#2588=EDGE_LOOP('',(#8350));
#3100=CIRCLE('',#11346,0.17);
#3101=CIRCLE('',#11348,0.1954);
#3102=CIRCLE('',#11350,0.1954);
#3103=CIRCLE('',#11352,0.125);
#3662=LINE('',#18570,#4266);
#3663=LINE('',#18572,#4267);
#3664=LINE('',#18574,#4268);
#3665=LINE('',#18575,#4269);
#3666=LINE('',#18578,#4270);
#3667=LINE('',#18580,#4271);
#3668=LINE('',#18581,#4272);
#3669=LINE('',#18584,#4273);
#3670=LINE('',#18586,#4274);
#3671=LINE('',#18587,#4275);
#3672=LINE('',#18590,#4276);
#3673=LINE('',#18592,#4277);
#3674=LINE('',#18593,#4278);
#3675=LINE('',#18596,#4279);
#3676=LINE('',#18598,#4280);
#3677=LINE('',#18599,#4281);
#3678=LINE('',#18601,#4282);
#3679=LINE('',#18602,#4283);
#3680=LINE('',#18610,#4284);
#3681=LINE('',#18614,#4285);
#3682=LINE('',#18618,#4286);
#4266=VECTOR('',#14202,1.);
#4267=VECTOR('',#14203,1.);
#4268=VECTOR('',#14204,1.);
#4269=VECTOR('',#14205,1.);
#4270=VECTOR('',#14208,1.);
#4271=VECTOR('',#14209,1.);
#4272=VECTOR('',#14210,1.);
#4273=VECTOR('',#14213,1.);
#4274=VECTOR('',#14214,1.);
#4275=VECTOR('',#14215,1.);
#4276=VECTOR('',#14218,1.);
#4277=VECTOR('',#14219,1.);
#4278=VECTOR('',#14220,1.);
#4279=VECTOR('',#14223,1.);
#4280=VECTOR('',#14224,1.);
#4281=VECTOR('',#14225,1.);
#4282=VECTOR('',#14228,1.);
#4283=VECTOR('',#14229,1.);
#4284=VECTOR('',#14240,0.185);
#4285=VECTOR('',#14245,0.2);
#4286=VECTOR('',#14250,0.1625);
#5034=VERTEX_POINT('',#18568);
#5035=VERTEX_POINT('',#18569);
#5036=VERTEX_POINT('',#18571);
#5037=VERTEX_POINT('',#18573);
#5038=VERTEX_POINT('',#18577);
#5039=VERTEX_POINT('',#18579);
#5040=VERTEX_POINT('',#18583);
#5041=VERTEX_POINT('',#18585);
#5042=VERTEX_POINT('',#18589);
#5043=VERTEX_POINT('',#18591);
#5044=VERTEX_POINT('',#18595);
#5045=VERTEX_POINT('',#18597);
#5046=VERTEX_POINT('',#18605);
#5047=VERTEX_POINT('',#18608);
#5048=VERTEX_POINT('',#18612);
#5049=VERTEX_POINT('',#18616);
#6137=EDGE_CURVE('',#5034,#5035,#3662,.T.);
#6138=EDGE_CURVE('',#5034,#5036,#3663,.T.);
#6139=EDGE_CURVE('',#5036,#5037,#3664,.T.);
#6140=EDGE_CURVE('',#5035,#5037,#3665,.T.);
#6141=EDGE_CURVE('',#5038,#5034,#3666,.T.);
#6142=EDGE_CURVE('',#5038,#5039,#3667,.T.);
#6143=EDGE_CURVE('',#5039,#5036,#3668,.T.);
#6144=EDGE_CURVE('',#5040,#5038,#3669,.T.);
#6145=EDGE_CURVE('',#5040,#5041,#3670,.T.);
#6146=EDGE_CURVE('',#5041,#5039,#3671,.T.);
#6147=EDGE_CURVE('',#5042,#5040,#3672,.T.);
#6148=EDGE_CURVE('',#5042,#5043,#3673,.T.);
#6149=EDGE_CURVE('',#5043,#5041,#3674,.T.);
#6150=EDGE_CURVE('',#5044,#5042,#3675,.T.);
#6151=EDGE_CURVE('',#5044,#5045,#3676,.T.);
#6152=EDGE_CURVE('',#5045,#5043,#3677,.T.);
#6153=EDGE_CURVE('',#5035,#5044,#3678,.T.);
#6154=EDGE_CURVE('',#5037,#5045,#3679,.T.);
#6155=EDGE_CURVE('',#5046,#5046,#3100,.T.);
#6156=EDGE_CURVE('',#5047,#5047,#3101,.T.);
#6157=EDGE_CURVE('',#5047,#5046,#3680,.T.);
#6158=EDGE_CURVE('',#5048,#5048,#3102,.F.);
#6159=EDGE_CURVE('',#5048,#5047,#3681,.T.);
#6160=EDGE_CURVE('',#5049,#5049,#3103,.T.);
#6161=EDGE_CURVE('',#5049,#5048,#3682,.T.);
#8301=ORIENTED_EDGE('',*,*,#6137,.F.);
#8302=ORIENTED_EDGE('',*,*,#6138,.T.);
#8303=ORIENTED_EDGE('',*,*,#6139,.T.);
#8304=ORIENTED_EDGE('',*,*,#6140,.F.);
#8305=ORIENTED_EDGE('',*,*,#6141,.F.);
#8306=ORIENTED_EDGE('',*,*,#6142,.T.);
#8307=ORIENTED_EDGE('',*,*,#6143,.T.);
#8308=ORIENTED_EDGE('',*,*,#6138,.F.);
#8309=ORIENTED_EDGE('',*,*,#6144,.F.);
#8310=ORIENTED_EDGE('',*,*,#6145,.T.);
#8311=ORIENTED_EDGE('',*,*,#6146,.T.);
#8312=ORIENTED_EDGE('',*,*,#6142,.F.);
#8313=ORIENTED_EDGE('',*,*,#6147,.F.);
#8314=ORIENTED_EDGE('',*,*,#6148,.T.);
#8315=ORIENTED_EDGE('',*,*,#6149,.T.);
#8316=ORIENTED_EDGE('',*,*,#6145,.F.);
#8317=ORIENTED_EDGE('',*,*,#6150,.F.);
#8318=ORIENTED_EDGE('',*,*,#6151,.T.);
#8319=ORIENTED_EDGE('',*,*,#6152,.T.);
#8320=ORIENTED_EDGE('',*,*,#6148,.F.);
#8321=ORIENTED_EDGE('',*,*,#6153,.F.);
#8322=ORIENTED_EDGE('',*,*,#6140,.T.);
#8323=ORIENTED_EDGE('',*,*,#6154,.T.);
#8324=ORIENTED_EDGE('',*,*,#6151,.F.);
#8325=ORIENTED_EDGE('',*,*,#6154,.F.);
#8326=ORIENTED_EDGE('',*,*,#6139,.F.);
#8327=ORIENTED_EDGE('',*,*,#6143,.F.);
#8328=ORIENTED_EDGE('',*,*,#6146,.F.);
#8329=ORIENTED_EDGE('',*,*,#6149,.F.);
#8330=ORIENTED_EDGE('',*,*,#6152,.F.);
#8331=ORIENTED_EDGE('',*,*,#6155,.F.);
#8332=ORIENTED_EDGE('',*,*,#6137,.T.);
#8333=ORIENTED_EDGE('',*,*,#6153,.T.);
#8334=ORIENTED_EDGE('',*,*,#6150,.T.);
#8335=ORIENTED_EDGE('',*,*,#6147,.T.);
#8336=ORIENTED_EDGE('',*,*,#6144,.T.);
#8337=ORIENTED_EDGE('',*,*,#6141,.T.);
#8338=ORIENTED_EDGE('',*,*,#6156,.F.);
#8339=ORIENTED_EDGE('',*,*,#6157,.T.);
#8340=ORIENTED_EDGE('',*,*,#6155,.T.);
#8341=ORIENTED_EDGE('',*,*,#6157,.F.);
#8342=ORIENTED_EDGE('',*,*,#6158,.F.);
#8343=ORIENTED_EDGE('',*,*,#6159,.T.);
#8344=ORIENTED_EDGE('',*,*,#6156,.T.);
#8345=ORIENTED_EDGE('',*,*,#6159,.F.);
#8346=ORIENTED_EDGE('',*,*,#6160,.F.);
#8347=ORIENTED_EDGE('',*,*,#6161,.T.);
#8348=ORIENTED_EDGE('',*,*,#6158,.T.);
#8349=ORIENTED_EDGE('',*,*,#6161,.F.);
#8350=ORIENTED_EDGE('',*,*,#6160,.T.);
#8852=PLANE('',#11338);
#8853=PLANE('',#11339);
#8854=PLANE('',#11340);
#8855=PLANE('',#11341);
#8856=PLANE('',#11342);
#8857=PLANE('',#11343);
#8858=PLANE('',#11344);
#8859=PLANE('',#11345);
#8860=PLANE('',#11353);
#9401=ADVANCED_FACE('',(#1796),#8852,.F.);
#9402=ADVANCED_FACE('',(#1797),#8853,.F.);
#9403=ADVANCED_FACE('',(#1798),#8854,.F.);
#9404=ADVANCED_FACE('',(#1799),#8855,.F.);
#9405=ADVANCED_FACE('',(#1800),#8856,.F.);
#9406=ADVANCED_FACE('',(#1801),#8857,.F.);
#9407=ADVANCED_FACE('',(#1802),#8858,.F.);
#9408=ADVANCED_FACE('',(#1803,#1032),#8859,.T.);
#9409=ADVANCED_FACE('',(#1804),#548,.T.);
#9410=ADVANCED_FACE('',(#1805),#1271,.T.);
#9411=ADVANCED_FACE('',(#1806),#549,.T.);
#9412=ADVANCED_FACE('',(#1807),#8860,.T.);
#9539=CLOSED_SHELL('',(#9401,#9402,#9403,#9404,#9405,#9406,#9407,#9408,
#9409,#9410,#9411,#9412));
#11337=AXIS2_PLACEMENT_3D('',#18566,#14198,#14199);
#11338=AXIS2_PLACEMENT_3D('',#18567,#14200,#14201);
#11339=AXIS2_PLACEMENT_3D('',#18576,#14206,#14207);
#11340=AXIS2_PLACEMENT_3D('',#18582,#14211,#14212);
#11341=AXIS2_PLACEMENT_3D('',#18588,#14216,#14217);
#11342=AXIS2_PLACEMENT_3D('',#18594,#14221,#14222);
#11343=AXIS2_PLACEMENT_3D('',#18600,#14226,#14227);
#11344=AXIS2_PLACEMENT_3D('',#18603,#14230,#14231);
#11345=AXIS2_PLACEMENT_3D('',#18604,#14232,#14233);
#11346=AXIS2_PLACEMENT_3D('',#18606,#14234,#14235);
#11347=AXIS2_PLACEMENT_3D('',#18607,#14236,#14237);
#11348=AXIS2_PLACEMENT_3D('',#18609,#14238,#14239);
#11349=AXIS2_PLACEMENT_3D('',#18611,#14241,#14242);
#11350=AXIS2_PLACEMENT_3D('',#18613,#14243,#14244);
#11351=AXIS2_PLACEMENT_3D('',#18615,#14246,#14247);
#11352=AXIS2_PLACEMENT_3D('',#18617,#14248,#14249);
#11353=AXIS2_PLACEMENT_3D('',#18619,#14251,#14252);
#14198=DIRECTION('axis',(0.,0.,1.));
#14199=DIRECTION('refdir',(1.,0.,0.));
#14200=DIRECTION('center_axis',(0.866025403784439,0.,-0.5));
#14201=DIRECTION('ref_axis',(0.5,0.,0.866025403784439));
#14202=DIRECTION('',(0.5,0.,0.866025403784439));
#14203=DIRECTION('',(0.,-1.,0.));
#14204=DIRECTION('',(0.5,0.,0.866025403784439));
#14205=DIRECTION('',(0.,-1.,0.));
#14206=DIRECTION('center_axis',(1.20185167898973E-16,0.,-1.));
#14207=DIRECTION('ref_axis',(1.,0.,1.20185167898973E-16));
#14208=DIRECTION('',(1.,0.,1.20185167898973E-16));
#14209=DIRECTION('',(0.,-1.,0.));
#14210=DIRECTION('',(1.,0.,1.20185167898973E-16));
#14211=DIRECTION('center_axis',(-0.866025403784439,0.,-0.5));
#14212=DIRECTION('ref_axis',(0.5,0.,-0.866025403784439));
#14213=DIRECTION('',(0.5,0.,-0.866025403784439));
#14214=DIRECTION('',(0.,-1.,0.));
#14215=DIRECTION('',(0.5,0.,-0.866025403784439));
#14216=DIRECTION('center_axis',(-0.866025403784439,0.,0.5));
#14217=DIRECTION('ref_axis',(-0.5,0.,-0.866025403784439));
#14218=DIRECTION('',(-0.5,0.,-0.866025403784439));
#14219=DIRECTION('',(0.,-1.,0.));
#14220=DIRECTION('',(-0.5,0.,-0.866025403784439));
#14221=DIRECTION('center_axis',(-2.40370335797945E-16,0.,1.));
#14222=DIRECTION('ref_axis',(-1.,0.,-2.40370335797945E-16));
#14223=DIRECTION('',(-1.,0.,-2.40370335797945E-16));
#14224=DIRECTION('',(0.,-1.,0.));
#14225=DIRECTION('',(-1.,0.,-2.40370335797945E-16));
#14226=DIRECTION('center_axis',(0.866025403784439,0.,0.5));
#14227=DIRECTION('ref_axis',(-0.5,0.,0.866025403784439));
#14228=DIRECTION('',(-0.5,0.,0.866025403784439));
#14229=DIRECTION('',(-0.5,0.,0.866025403784439));
#14230=DIRECTION('center_axis',(0.,-1.,0.));
#14231=DIRECTION('ref_axis',(0.,0.,-1.));
#14232=DIRECTION('center_axis',(0.,1.,0.));
#14233=DIRECTION('ref_axis',(0.,0.,1.));
#14234=DIRECTION('center_axis',(0.,-1.,0.));
#14235=DIRECTION('ref_axis',(1.,0.,0.));
#14236=DIRECTION('center_axis',(0.,-1.,0.));
#14237=DIRECTION('ref_axis',(1.,0.,0.));
#14238=DIRECTION('center_axis',(0.,-1.,0.));
#14239=DIRECTION('ref_axis',(1.,0.,0.));
#14240=DIRECTION('',(0.707106781186548,0.707106781186547,8.65956056235494E-17));
#14241=DIRECTION('center_axis',(0.,-1.,0.));
#14242=DIRECTION('ref_axis',(1.,0.,0.));
#14243=DIRECTION('center_axis',(0.,1.,0.));
#14244=DIRECTION('ref_axis',(1.,0.,0.));
#14245=DIRECTION('',(0.,1.,0.));
#14246=DIRECTION('center_axis',(0.,1.,0.));
#14247=DIRECTION('ref_axis',(1.,0.,0.));
#14248=DIRECTION('center_axis',(0.,-1.,0.));
#14249=DIRECTION('ref_axis',(1.,0.,0.));
#14250=DIRECTION('',(-0.707106781186548,0.707106781186547,-8.65956056235494E-17));
#14251=DIRECTION('center_axis',(0.,-1.,0.));
#14252=DIRECTION('ref_axis',(0.,0.,-1.));
#18566=CARTESIAN_POINT('',(0.,0.,0.));
#18567=CARTESIAN_POINT('Origin',(0.0577350269189626,0.,-0.1));
#18568=CARTESIAN_POINT('',(0.0577350269189626,0.,-0.1));
#18569=CARTESIAN_POINT('',(0.115470053837925,0.,0.));
#18570=CARTESIAN_POINT('',(0.0934187836487032,0.,-0.0381939203391614));
#18571=CARTESIAN_POINT('',(0.0577350269189626,-0.2,-0.1));
#18572=CARTESIAN_POINT('',(0.0577350269189626,0.,-0.1));
#18573=CARTESIAN_POINT('',(0.115470053837925,-0.2,0.));
#18574=CARTESIAN_POINT('',(0.115470053837925,-0.2,0.));
#18575=CARTESIAN_POINT('',(0.115470053837925,0.,0.));
#18576=CARTESIAN_POINT('Origin',(-0.0577350269189626,0.,-0.1));
#18577=CARTESIAN_POINT('',(-0.0577350269189626,0.,-0.1));
#18578=CARTESIAN_POINT('',(0.0561324865405187,0.,-0.1));
#18579=CARTESIAN_POINT('',(-0.0577350269189626,-0.2,-0.1));
#18580=CARTESIAN_POINT('',(-0.0577350269189626,0.,-0.1));
#18581=CARTESIAN_POINT('',(0.0577350269189626,-0.2,-0.1));
#18582=CARTESIAN_POINT('Origin',(-0.115470053837925,0.,-1.38777878078145E-17));
#18583=CARTESIAN_POINT('',(-0.115470053837925,0.,-1.41410031829988E-17));
#18584=CARTESIAN_POINT('',(-0.0797862971081845,0.,-0.0618060796608387));
#18585=CARTESIAN_POINT('',(-0.115470053837925,-0.2,-1.38777878078145E-17));
#18586=CARTESIAN_POINT('',(-0.115470053837925,0.,-1.41410031829988E-17));
#18587=CARTESIAN_POINT('',(-0.0577350269189626,-0.2,-0.1));
#18588=CARTESIAN_POINT('Origin',(-0.0577350269189626,0.,0.1));
#18589=CARTESIAN_POINT('',(-0.0577350269189626,0.,0.1));
#18590=CARTESIAN_POINT('',(-0.0509187836487033,0.,0.111806079660839));
#18591=CARTESIAN_POINT('',(-0.0577350269189626,-0.2,0.1));
#18592=CARTESIAN_POINT('',(-0.0577350269189626,0.,0.1));
#18593=CARTESIAN_POINT('',(-0.115470053837925,-0.2,-1.41410031829988E-17));
#18594=CARTESIAN_POINT('Origin',(0.0577350269189626,0.,0.1));
#18595=CARTESIAN_POINT('',(0.0577350269189626,0.,0.1));
#18596=CARTESIAN_POINT('',(0.113867513459481,0.,0.1));
#18597=CARTESIAN_POINT('',(0.0577350269189626,-0.2,0.1));
#18598=CARTESIAN_POINT('',(0.0577350269189626,0.,0.1));
#18599=CARTESIAN_POINT('',(-0.0577350269189626,-0.2,0.1));
#18600=CARTESIAN_POINT('Origin',(0.115470053837925,0.,0.));
#18601=CARTESIAN_POINT('',(0.122286297108185,0.,-0.0118060796608386));
#18602=CARTESIAN_POINT('',(0.0577350269189626,-0.2,0.1));
#18603=CARTESIAN_POINT('Origin',(0.,-0.2,0.));
#18604=CARTESIAN_POINT('Origin',(0.17,0.,0.));
#18605=CARTESIAN_POINT('',(-0.17,-8.67361737988404E-18,-2.0818995585505E-17));
#18606=CARTESIAN_POINT('Origin',(0.,0.,0.));
#18607=CARTESIAN_POINT('Origin',(0.,-0.015,0.));
#18608=CARTESIAN_POINT('',(-0.1954,-0.0254,-2.39295984553393E-17));
#18609=CARTESIAN_POINT('Origin',(0.,-0.0254,0.));
#18610=CARTESIAN_POINT('',(-0.185,-0.015,-2.2655965784226E-17));
#18611=CARTESIAN_POINT('Origin',(0.,-0.2775,0.));
#18612=CARTESIAN_POINT('',(-0.1954,-0.5296,2.39295984553393E-17));
#18613=CARTESIAN_POINT('Origin',(0.,-0.5296,0.));
#18614=CARTESIAN_POINT('',(-0.1954,-0.2775,-2.39295984553393E-17));
#18615=CARTESIAN_POINT('Origin',(0.,-0.5625,0.));
#18616=CARTESIAN_POINT('',(-0.125,-0.6,-1.53080849893419E-17));
#18617=CARTESIAN_POINT('Origin',(0.,-0.6,0.));
#18618=CARTESIAN_POINT('',(-0.1625,-0.5625,-1.99005104861445E-17));
#18619=CARTESIAN_POINT('Origin',(0.,-0.6,0.));
#18963=UNCERTAINTY_MEASURE_WITH_UNIT(LENGTH_MEASURE(0.001),#19044,
'DISTANCE_ACCURACY_VALUE',
'Maximum model space distance between geometric entities at asserted c
onnectivities');
#18972=UNCERTAINTY_MEASURE_WITH_UNIT(LENGTH_MEASURE(0.001),#19044,
'DISTANCE_ACCURACY_VALUE',
'Maximum model space distance between geometric entities at asserted c
onnectivities');
#19034=(
GEOMETRIC_REPRESENTATION_CONTEXT(3)
GLOBAL_UNCERTAINTY_ASSIGNED_CONTEXT((#18963))
GLOBAL_UNIT_ASSIGNED_CONTEXT((#19044,#19046,#19047))
REPRESENTATION_CONTEXT('','3D')
);
#19043=(
GEOMETRIC_REPRESENTATION_CONTEXT(3)
GLOBAL_UNCERTAINTY_ASSIGNED_CONTEXT((#18972))
GLOBAL_UNIT_ASSIGNED_CONTEXT((#19044,#19046,#19047))
REPRESENTATION_CONTEXT('','3D')
);
#19044=(
LENGTH_UNIT()
NAMED_UNIT(*)
SI_UNIT(.CENTI.,.METRE.)
);
#19046=(
NAMED_UNIT(*)
PLANE_ANGLE_UNIT()
SI_UNIT($,.RADIAN.)
);
#19047=(
NAMED_UNIT(*)
SI_UNIT($,.STERADIAN.)
SOLID_ANGLE_UNIT()
);
#19109=SHAPE_DEFINITION_REPRESENTATION(#19266,#19367);
#19266=PRODUCT_DEFINITION_SHAPE('',$,#19438);
#19367=SHAPE_REPRESENTATION('',(#11337),#19034);
#19376=PRODUCT_DEFINITION_CONTEXT('part definition',#19588,'design');
#19438=PRODUCT_DEFINITION('2026-11-03-00-38-46-517',
'Socket Set Screw - M4x6',#19508,#19376);
#19508=PRODUCT_DEFINITION_FORMATION('',$,#19651);
#19588=APPLICATION_CONTEXT(
'Core Data for Automotive Mechanical Design Process');
#19589=PRODUCT_CONTEXT('part definition',#19588,'mechanical');
#19651=PRODUCT('2026-11-03-00-38-46-517','Socket Set Screw - M4x6',
'Socket Set Screw - M4x6',(#19589));
#19663=PRESENTATION_STYLE_ASSIGNMENT((#19669));
#19669=SURFACE_STYLE_USAGE(.BOTH.,#19675);
#19675=SURFACE_SIDE_STYLE('',(#19681));
#19681=SURFACE_STYLE_FILL_AREA(#19687);
#19687=FILL_AREA_STYLE('CAD Library Painted - Graphite',(#19693));
#19693=FILL_AREA_STYLE_COLOUR('CAD Library Painted - Graphite',#19699);
#19699=COLOUR_RGB('CAD Library Painted - Graphite',0.168627450980392,0.192156862745098,
0.231372549019608);
ENDSEC;
END-ISO-10303-21;
